ISO-10303-21;
HEADER;
FILE_DESCRIPTION (('STEP AP214'),
    '1' );
FILE_NAME ('Mechanical Shaft Face Seal.step',
    '2026-10-09T13:19:41',
    ( '' ),
    ( '' ),
    'SwSTEP 2.0',
    'SolidWorks 2026',
    '' );
FILE_SCHEMA (( 'AUTOMOTIVE_DESIGN' ));
ENDSEC;

DATA;
#260=FILL_AREA_STYLE_COLOUR ( '', #13962 ) ;
#302=CARTESIAN_POINT ( 'NONE',  ( -15.53338745080000116, -84.25000000000000000, -28.43367500519999780 ) ) ;
#324=ORIENTED_EDGE ( 'NONE', *, *, #4162, .T. ) ;
#359=LINE ( 'NONE', #9205, #7030 ) ;
#570=ORIENTED_EDGE ( 'NONE', *, *, #2545, .F. ) ;
#694=CIRCLE ( 'NONE', #26077, 1.249999999999999112 ) ;
#979=CYLINDRICAL_SURFACE ( 'NONE', #11270, 32.39999999999999147 ) ;
#1037=ORIENTED_EDGE ( 'NONE', *, *, #28166, .F. ) ;
#1256=EDGE_CURVE ( 'NONE', #22342, #8389, #23961, .T. ) ;
#1285=ORIENTED_EDGE ( 'NONE', *, *, #14765, .T. ) ;
#1324=CARTESIAN_POINT ( 'NONE',  ( 0.000000000000000000, -84.75000000000000000, 0.000000000000000000 ) ) ;
#1417=STYLED_ITEM ( 'NONE', ( #26599 ), #15528 ) ;
#1584=AXIS2_PLACEMENT_3D ( 'NONE', #14440, #21562, #16910 ) ;
#1824=TOROIDAL_SURFACE ( 'NONE', #18111, 33.64999999999999858, 1.250000000000000000 ) ;
#2112=FACE_OUTER_BOUND ( 'NONE', #6314, .T. ) ;
#2117=AXIS2_PLACEMENT_3D ( 'NONE', #18371, #11937, #5104 ) ;
#2131=SURFACE_SIDE_STYLE ('',( #22672 ) ) ;
#2199=ADVANCED_FACE ( 'NONE', ( #10441 ), #18294, .T. ) ;
#2413=EDGE_LOOP ( 'NONE', ( #27282, #9515, #27107, #1037 ) ) ;
#2432=CARTESIAN_POINT ( 'NONE',  ( 15.53338745080000116, -84.75000000000000000, 28.43367500519999780 ) ) ;
#2545=EDGE_CURVE ( 'NONE', #20314, #20323, #27932, .T. ) ;
#2683=ORIENTED_EDGE ( 'NONE', *, *, #13823, .F. ) ;
#2699=DIRECTION ( 'NONE',  ( -0.8775825618903722036, 0.000000000000000000, 0.4794255386042041156 ) ) ;
#3087=ORIENTED_EDGE ( 'NONE', *, *, #16278, .T. ) ;
#3228=DIRECTION ( 'NONE',  ( 0.000000000000000000, 1.000000000000000000, 0.000000000000000000 ) ) ;
#3293=EDGE_LOOP ( 'NONE', ( #2683, #25707, #25641, #5766 ) ) ;
#3329=CARTESIAN_POINT ( 'NONE',  ( -16.73195129730000374, -84.25000000000000000, -30.62763141000000289 ) ) ;
#3387=AXIS2_PLACEMENT_3D ( 'NONE', #4443, #4737, #4885 ) ;
#3498=CARTESIAN_POINT ( 'NONE',  ( 0.000000000000000000, -83.75000000000000000, 0.000000000000000000 ) ) ;
#3652=ADVANCED_FACE ( 'NONE', ( #23182 ), #1824, .T. ) ;
#3654=ADVANCED_FACE ( 'NONE', ( #5404 ), #27568, .F. ) ;
#3731=CARTESIAN_POINT ( 'NONE',  ( 16.73195129730000374, -84.75000000000000000, 30.62763141000000289 ) ) ;
#3738=DIRECTION ( 'NONE',  ( 0.000000000000000000, 1.000000000000000000, 0.000000000000000000 ) ) ;
#3857=DIRECTION ( 'NONE',  ( 0.8775825618903722036, 0.000000000000000000, -0.4794255386042041156 ) ) ;
#3858=PRODUCT_DEFINITION_SHAPE ( 'NONE', 'NONE',  #4003 ) ;
#4003=PRODUCT_DEFINITION ( 'UNKNOWN', '', #19919, #4811 ) ;
#4162=EDGE_CURVE ( 'NONE', #5957, #12729, #26421, .T. ) ;
#4374=AXIS2_PLACEMENT_3D ( 'NONE', #21491, #3857, #24532 ) ;
#4443=CARTESIAN_POINT ( 'NONE',  ( 0.000000000000000000, -84.75000000000000000, 0.000000000000000000 ) ) ;
#4513=ORIENTED_EDGE ( 'NONE', *, *, #4162, .F. ) ;
#4737=DIRECTION ( 'NONE',  ( 0.000000000000000000, 1.000000000000000000, 0.000000000000000000 ) ) ;
#4811=PRODUCT_DEFINITION_CONTEXT ( 'detailed design', #10323, 'design' ) ;
#4877=DIRECTION ( 'NONE',  ( 1.000000000000000000, 0.000000000000000000, 0.000000000000000000 ) ) ;
#4885=DIRECTION ( 'NONE',  ( 1.000000000000000000, 0.000000000000000000, 0.000000000000000000 ) ) ;
#4974=CARTESIAN_POINT ( 'NONE',  ( 0.000000000000000000, -84.75000000000000000, 0.000000000000000000 ) ) ;
#5053=( GEOMETRIC_REPRESENTATION_CONTEXT ( 3 ) GLOBAL_UNCERTAINTY_ASSIGNED_CONTEXT ( ( #18800 ) ) GLOBAL_UNIT_ASSIGNED_CONTEXT ( ( #5697, #28128, #23755 ) ) REPRESENTATION_CONTEXT ( 'NONE', 'WORKASPACE' ) );
#5104=DIRECTION ( 'NONE',  ( 1.000000000000000000, 0.000000000000000000, 0.000000000000000000 ) ) ;
#5303=DIRECTION ( 'NONE',  ( 0.000000000000000000, 1.000000000000000000, 0.000000000000000000 ) ) ;
#5353=ADVANCED_BREP_SHAPE_REPRESENTATION ( '', ( #15528, #26433 ), #5053 ) ;
#5368=ADVANCED_FACE ( 'NONE', ( #16041 ), #21378, .T. ) ;
#5404=FACE_OUTER_BOUND ( 'NONE', #13817, .T. ) ;
#5459=DIRECTION ( 'NONE',  ( 0.000000000000000000, 1.000000000000000000, 0.000000000000000000 ) ) ;
#5562=DIRECTION ( 'NONE',  ( 0.000000000000000000, 0.000000000000000000, 1.000000000000000000 ) ) ;
#5599=FACE_OUTER_BOUND ( 'NONE', #28204, .T. ) ;
#5697=( LENGTH_UNIT ( ) NAMED_UNIT ( * ) SI_UNIT ( .MILLI., .METRE. ) );
#5766=ORIENTED_EDGE ( 'NONE', *, *, #18134, .F. ) ;
#5957=VERTEX_POINT ( 'NONE', #27433 ) ;
#6090=ORIENTED_EDGE ( 'NONE', *, *, #18097, .T. ) ;
#6314=EDGE_LOOP ( 'NONE', ( #4513, #3087, #24947, #11967 ) ) ;
#6324=DIRECTION ( 'NONE',  ( 1.000000000000000000, 0.000000000000000000, 0.000000000000000000 ) ) ;
#6507=ADVANCED_FACE ( 'NONE', ( #5599 ), #979, .F. ) ;
#6882=CARTESIAN_POINT ( 'NONE',  ( -16.73195129730000374, -84.75000000000000000, -30.62763141000000289 ) ) ;
#6967=AXIS2_PLACEMENT_3D ( 'NONE', #15051, #26737, #6324 ) ;
#7030=VECTOR ( 'NONE', #22337, 1000.000000000000000 ) ;
#7285=DIRECTION ( 'NONE',  ( 0.8775825618903722036, 0.000000000000000000, -0.4794255386042041156 ) ) ;
#8116=VERTEX_POINT ( 'NONE', #13188 ) ;
#8133=CARTESIAN_POINT ( 'NONE',  ( 16.73195129730000374, -83.75000000000000000, 30.62763141000000289 ) ) ;
#8160=CARTESIAN_POINT ( 'NONE',  ( -16.13266937400000245, -83.75000000000000000, -29.53065320760000034 ) ) ;
#8389=VERTEX_POINT ( 'NONE', #3731 ) ;
#8847=LINE ( 'NONE', #302, #26481 ) ;
#9205=CARTESIAN_POINT ( 'NONE',  ( 16.73195129730000374, -84.25000000000000000, 30.62763141000000289 ) ) ;
#9247=ORIENTED_EDGE ( 'NONE', *, *, #13823, .T. ) ;
#9515=ORIENTED_EDGE ( 'NONE', *, *, #19917, .T. ) ;
#9774=EDGE_CURVE ( 'NONE', #12729, #8389, #359, .T. ) ;
#10069=CARTESIAN_POINT ( 'NONE',  ( 0.000000000000000000, -83.75000000000000000, 0.000000000000000000 ) ) ;
#10233=AXIS2_PLACEMENT_3D ( 'NONE', #13153, #10945, #17107 ) ;
#10323=APPLICATION_CONTEXT ( 'automotive_design' ) ;
#10441=FACE_OUTER_BOUND ( 'NONE', #11443, .T. ) ;
#10587=AXIS2_PLACEMENT_3D ( 'NONE', #11332, #26357, #26650 ) ;
#10661=CYLINDRICAL_SURFACE ( 'NONE', #10233, 34.89999999999999858 ) ;
#10857=ORIENTED_EDGE ( 'NONE', *, *, #28166, .T. ) ;
#10945=DIRECTION ( 'NONE',  ( 0.000000000000000000, 1.000000000000000000, 0.000000000000000000 ) ) ;
#10969=FILL_AREA_STYLE ('',( #260 ) ) ;
#11265=ADVANCED_FACE ( 'NONE', ( #18178 ), #17283, .T. ) ;
#11270=AXIS2_PLACEMENT_3D ( 'NONE', #16531, #5459, #27884 ) ;
#11280=( LENGTH_UNIT ( ) NAMED_UNIT ( * ) SI_UNIT ( .MILLI., .METRE. ) );
#11286=CIRCLE ( 'NONE', #11781, 1.250000000000000000 ) ;
#11332=CARTESIAN_POINT ( 'NONE',  ( 0.000000000000000000, -84.75000000000000000, 0.000000000000000000 ) ) ;
#11443=EDGE_LOOP ( 'NONE', ( #21941, #10857, #324, #16398 ) ) ;
#11594=VERTEX_POINT ( 'NONE', #26229 ) ;
#11781=AXIS2_PLACEMENT_3D ( 'NONE', #21055, #2699, #25425 ) ;
#11804=CARTESIAN_POINT ( 'NONE',  ( 0.000000000000000000, -84.75000000000000000, 0.000000000000000000 ) ) ;
#11824=CIRCLE ( 'NONE', #17351, 32.39999999999999858 ) ;
#11921=CARTESIAN_POINT ( 'NONE',  ( 0.000000000000000000, -83.75000000000000000, 0.000000000000000000 ) ) ;
#11937=DIRECTION ( 'NONE',  ( 0.000000000000000000, 1.000000000000000000, 0.000000000000000000 ) ) ;
#11945=DIRECTION ( 'NONE',  ( 0.4794255386042040601, 0.000000000000000000, 0.8775825618903719816 ) ) ;
#11967=ORIENTED_EDGE ( 'NONE', *, *, #9774, .F. ) ;
#12005=APPLICATION_CONTEXT ( 'automotive_design' ) ;
#12729=VERTEX_POINT ( 'NONE', #8133 ) ;
#12791=DIRECTION ( 'NONE',  ( -0.8775825618903722036, 0.000000000000000000, 0.4794255386042041156 ) ) ;
#13044=CARTESIAN_POINT ( 'NONE',  ( 0.000000000000000000, -84.75000000000000000, 0.000000000000000000 ) ) ;
#13153=CARTESIAN_POINT ( 'NONE',  ( 0.000000000000000000, -84.75000000000000000, 0.000000000000000000 ) ) ;
#13188=CARTESIAN_POINT ( 'NONE',  ( -15.53338745080000116, -83.75000000000000000, -28.43367500519999780 ) ) ;
#13238=EDGE_CURVE ( 'NONE', #11594, #20314, #20391, .T. ) ;
#13239=UNCERTAINTY_MEASURE_WITH_UNIT (LENGTH_MEASURE( 1.000000000000000082E-05 ), #11280, 'distance_accuracy_value', 'NONE');
#13380=CARTESIAN_POINT ( 'NONE',  ( 16.13266937400000245, -83.75000000000000000, 29.53065320760000034 ) ) ;
#13384=SHAPE_DEFINITION_REPRESENTATION ( #3858, #19699 ) ;
#13717=DIRECTION ( 'NONE',  ( 0.000000000000000000, 1.000000000000000000, 0.000000000000000000 ) ) ;
#13817=EDGE_LOOP ( 'NONE', ( #17715, #1285, #6090, #570 ) ) ;
#13823=EDGE_CURVE ( 'NONE', #8389, #22342, #28322, .T. ) ;
#13902=CARTESIAN_POINT ( 'NONE',  ( 0.000000000000000000, -83.75000000000000000, 0.000000000000000000 ) ) ;
#13925=CIRCLE ( 'NONE', #6967, 32.39999999999999858 ) ;
#13962=COLOUR_RGB ( '', 0.31764706, 0.68627451, 0.89019608) ;
#14394=EDGE_CURVE ( 'NONE', #20323, #8116, #13925, .T. ) ;
#14440=CARTESIAN_POINT ( 'NONE',  ( 0.000000000000000000, -84.75000000000000000, 0.000000000000000000 ) ) ;
#14697=DIRECTION ( 'NONE',  ( 0.000000000000000000, 1.000000000000000000, 0.000000000000000000 ) ) ;
#14765=EDGE_CURVE ( 'NONE', #11594, #8116, #8847, .T. ) ;
#14772=PRODUCT ( 'Mechanical Shaft Face Seal', 'Mechanical Shaft Face Seal', '', ( #15569 ) ) ;
#15051=CARTESIAN_POINT ( 'NONE',  ( 0.000000000000000000, -83.75000000000000000, 0.000000000000000000 ) ) ;
#15080=AXIS2_PLACEMENT_3D ( 'NONE', #10069, #5303, #25688 ) ;
#15380=AXIS2_PLACEMENT_3D ( 'NONE', #24590, #20215, #28797 ) ;
#15528=MANIFOLD_SOLID_BREP ( 'O-Ring Seal', #20743 ) ;
#15569=PRODUCT_CONTEXT ( 'NONE', #12005, 'mechanical' ) ;
#15773=AXIS2_PLACEMENT_3D ( 'NONE', #4974, #13717, #16183 ) ;
#15951=( NAMED_UNIT ( * ) SI_UNIT ( $, .STERADIAN. ) SOLID_ANGLE_UNIT ( ) );
#16041=FACE_OUTER_BOUND ( 'NONE', #26630, .T. ) ;
#16183=DIRECTION ( 'NONE',  ( 0.4794255386042040601, 0.000000000000000000, 0.8775825618903719816 ) ) ;
#16278=EDGE_CURVE ( 'NONE', #5957, #22342, #16280, .T. ) ;
#16280=LINE ( 'NONE', #3329, #22554 ) ;
#16398=ORIENTED_EDGE ( 'NONE', *, *, #19917, .F. ) ;
#16531=CARTESIAN_POINT ( 'NONE',  ( 0.000000000000000000, -84.75000000000000000, 0.000000000000000000 ) ) ;
#16577=DIRECTION ( 'NONE',  ( 0.000000000000000000, -1.000000000000000000, 0.000000000000000000 ) ) ;
#16585=DIRECTION ( 'NONE',  ( 1.000000000000000000, 0.000000000000000000, 0.000000000000000000 ) ) ;
#16722=EDGE_CURVE ( 'NONE', #12729, #5957, #20224, .T. ) ;
#16910=DIRECTION ( 'NONE',  ( 0.4794255386042040601, 0.000000000000000000, 0.8775825618903719816 ) ) ;
#17107=DIRECTION ( 'NONE',  ( 0.4794255386042040601, 0.000000000000000000, 0.8775825618903719816 ) ) ;
#17195=ORIENTED_EDGE ( 'NONE', *, *, #2545, .T. ) ;
#17283=TOROIDAL_SURFACE ( 'NONE', #15380, 33.64999999999999858, 1.250000000000000000 ) ;
#17336=SHAPE_REPRESENTATION_RELATIONSHIP ( 'NONE' , 'NONE' ,  #19699, #5353 ) ;
#17351=AXIS2_PLACEMENT_3D ( 'NONE', #13902, #18724, #4877 ) ;
#17376=ADVANCED_FACE ( 'NONE', ( #25935 ), #25662, .T. ) ;
#17440=DIRECTION ( 'NONE',  ( 1.000000000000000000, 0.000000000000000000, 0.000000000000000000 ) ) ;
#17555=EDGE_LOOP ( 'NONE', ( #25399, #26331, #9247, #21180 ) ) ;
#17579=AXIS2_PLACEMENT_3D ( 'NONE', #11921, #18490, #16585 ) ;
#17715=ORIENTED_EDGE ( 'NONE', *, *, #13238, .F. ) ;
#18097=EDGE_CURVE ( 'NONE', #8116, #20323, #11824, .T. ) ;
#18111=AXIS2_PLACEMENT_3D ( 'NONE', #1324, #14697, #11945 ) ;
#18134=EDGE_CURVE ( 'NONE', #22342, #11594, #11286, .T. ) ;
#18178=FACE_OUTER_BOUND ( 'NONE', #2413, .T. ) ;
#18294=TOROIDAL_SURFACE ( 'NONE', #21092, 33.64999999999999858, 1.250000000000000000 ) ;
#18371=CARTESIAN_POINT ( 'NONE',  ( 0.000000000000000000, -84.75000000000000000, 0.000000000000000000 ) ) ;
#18490=DIRECTION ( 'NONE',  ( 0.000000000000000000, 1.000000000000000000, 0.000000000000000000 ) ) ;
#18724=DIRECTION ( 'NONE',  ( 0.000000000000000000, 1.000000000000000000, 0.000000000000000000 ) ) ;
#18742=CIRCLE ( 'NONE', #3387, 32.39999999999999858 ) ;
#18800=UNCERTAINTY_MEASURE_WITH_UNIT (LENGTH_MEASURE( 1.000000000000000082E-05 ), #5697, 'distance_accuracy_value', 'NONE');
#19216=DIRECTION ( 'NONE',  ( 0.000000000000000000, 1.000000000000000000, 0.000000000000000000 ) ) ;
#19336=ORIENTED_EDGE ( 'NONE', *, *, #13238, .T. ) ;
#19693=EDGE_CURVE ( 'NONE', #8389, #20314, #28551, .T. ) ;
#19699=SHAPE_REPRESENTATION ( 'Mechanical Shaft Face Seal', ( #26433 ), #5053 ) ;
#19917=EDGE_CURVE ( 'NONE', #20323, #12729, #694, .T. ) ;
#19919=PRODUCT_DEFINITION_FORMATION_WITH_SPECIFIED_SOURCE ( 'ANY', '', #14772, .NOT_KNOWN. ) ;
#19934=AXIS2_PLACEMENT_3D ( 'NONE', #13044, #26915, #17440 ) ;
#19938=DIRECTION ( 'NONE',  ( 0.4794255386042032829, 0.000000000000000000, 0.8775825618903726477 ) ) ;
#20002=MECHANICAL_DESIGN_GEOMETRIC_PRESENTATION_REPRESENTATION('',(#1417),#25150);
#20215=DIRECTION ( 'NONE',  ( 0.000000000000000000, 1.000000000000000000, 0.000000000000000000 ) ) ;
#20224=CIRCLE ( 'NONE', #15080, 34.89999999999999858 ) ;
#20314=VERTEX_POINT ( 'NONE', #2432 ) ;
#20323=VERTEX_POINT ( 'NONE', #26906 ) ;
#20391=CIRCLE ( 'NONE', #10587, 32.39999999999999858 ) ;
#20404=ADVANCED_FACE ( 'NONE', ( #2112 ), #10661, .T. ) ;
#20716=DIRECTION ( 'NONE',  ( 0.4794255386042041156, 0.000000000000000000, 0.8775825618903722036 ) ) ;
#20743=CLOSED_SHELL ( 'NONE', ( #2199, #3654, #20404, #11265, #6507, #5368, #17376, #3652 ) ) ;
#21044=ORIENTED_EDGE ( 'NONE', *, *, #14765, .F. ) ;
#21055=CARTESIAN_POINT ( 'NONE',  ( -16.13266937400000245, -84.75000000000000000, -29.53065320760000034 ) ) ;
#21092=AXIS2_PLACEMENT_3D ( 'NONE', #3498, #19216, #21266 ) ;
#21180=ORIENTED_EDGE ( 'NONE', *, *, #16278, .F. ) ;
#21266=DIRECTION ( 'NONE',  ( 0.4794255386042040601, 0.000000000000000000, 0.8775825618903719816 ) ) ;
#21378=TOROIDAL_SURFACE ( 'NONE', #15773, 33.64999999999999858, 1.250000000000000000 ) ;
#21491=CARTESIAN_POINT ( 'NONE',  ( 16.13266937400000245, -84.75000000000000000, 29.53065320760000034 ) ) ;
#21562=DIRECTION ( 'NONE',  ( 0.000000000000000000, 1.000000000000000000, 0.000000000000000000 ) ) ;
#21819=ORIENTED_EDGE ( 'NONE', *, *, #22719, .F. ) ;
#21941=ORIENTED_EDGE ( 'NONE', *, *, #18097, .F. ) ;
#21983=DIRECTION ( 'NONE',  ( 0.000000000000000000, 1.000000000000000000, 0.000000000000000000 ) ) ;
#22337=DIRECTION ( 'NONE',  ( 0.000000000000000000, -1.000000000000000000, 0.000000000000000000 ) ) ;
#22342=VERTEX_POINT ( 'NONE', #6882 ) ;
#22554=VECTOR ( 'NONE', #16577, 1000.000000000000000 ) ;
#22672=SURFACE_STYLE_FILL_AREA ( #10969 ) ;
#22719=EDGE_CURVE ( 'NONE', #20314, #11594, #18742, .T. ) ;
#23182=FACE_OUTER_BOUND ( 'NONE', #3293, .T. ) ;
#23616=AXIS2_PLACEMENT_3D ( 'NONE', #8160, #12791, #23746 ) ;
#23679=ORIENTED_EDGE ( 'NONE', *, *, #19693, .F. ) ;
#23746=DIRECTION ( 'NONE',  ( 0.4794255386042042266, 0.000000000000000000, 0.8775825618903720926 ) ) ;
#23755=( NAMED_UNIT ( * ) SI_UNIT ( $, .STERADIAN. ) SOLID_ANGLE_UNIT ( ) );
#23961=CIRCLE ( 'NONE', #2117, 34.89999999999999858 ) ;
#24163=ORIENTED_EDGE ( 'NONE', *, *, #18134, .T. ) ;
#24532=DIRECTION ( 'NONE',  ( 0.4794255386042032829, 0.000000000000000000, 0.8775825618903726477 ) ) ;
#24590=CARTESIAN_POINT ( 'NONE',  ( 0.000000000000000000, -83.75000000000000000, 0.000000000000000000 ) ) ;
#24710=SURFACE_STYLE_USAGE ( .BOTH. , #2131 ) ;
#24947=ORIENTED_EDGE ( 'NONE', *, *, #1256, .T. ) ;
#25150=( GEOMETRIC_REPRESENTATION_CONTEXT ( 3 ) GLOBAL_UNCERTAINTY_ASSIGNED_CONTEXT ( ( #13239 ) ) GLOBAL_UNIT_ASSIGNED_CONTEXT ( ( #11280, #28764, #15951 ) ) REPRESENTATION_CONTEXT ( 'NONE', 'WORKASPACE' ) );
#25255=DIRECTION ( 'NONE',  ( 1.000000000000000000, 0.000000000000000000, 0.000000000000000000 ) ) ;
#25399=ORIENTED_EDGE ( 'NONE', *, *, #16722, .F. ) ;
#25425=DIRECTION ( 'NONE',  ( 0.4794255386042042266, 0.000000000000000000, 0.8775825618903720926 ) ) ;
#25564=AXIS2_PLACEMENT_3D ( 'NONE', #11804, #3228, #20716 ) ;
#25641=ORIENTED_EDGE ( 'NONE', *, *, #22719, .T. ) ;
#25662=CYLINDRICAL_SURFACE ( 'NONE', #1584, 34.89999999999999858 ) ;
#25688=DIRECTION ( 'NONE',  ( 1.000000000000000000, 0.000000000000000000, 0.000000000000000000 ) ) ;
#25707=ORIENTED_EDGE ( 'NONE', *, *, #19693, .T. ) ;
#25935=FACE_OUTER_BOUND ( 'NONE', #17555, .T. ) ;
#26026=ORIENTED_EDGE ( 'NONE', *, *, #1256, .F. ) ;
#26077=AXIS2_PLACEMENT_3D ( 'NONE', #13380, #7285, #19938 ) ;
#26143=VECTOR ( 'NONE', #3738, 1000.000000000000000 ) ;
#26229=CARTESIAN_POINT ( 'NONE',  ( -15.53338745080000116, -84.75000000000000000, -28.43367500519999780 ) ) ;
#26331=ORIENTED_EDGE ( 'NONE', *, *, #9774, .T. ) ;
#26357=DIRECTION ( 'NONE',  ( 0.000000000000000000, 1.000000000000000000, 0.000000000000000000 ) ) ;
#26421=CIRCLE ( 'NONE', #17579, 34.89999999999999858 ) ;
#26433=AXIS2_PLACEMENT_3D ( 'NONE', #27589, #5562, #25255 ) ;
#26481=VECTOR ( 'NONE', #21983, 1000.000000000000000 ) ;
#26599=PRESENTATION_STYLE_ASSIGNMENT (( #24710 ) ) ;
#26630=EDGE_LOOP ( 'NONE', ( #26026, #24163, #19336, #23679 ) ) ;
#26650=DIRECTION ( 'NONE',  ( 1.000000000000000000, 0.000000000000000000, 0.000000000000000000 ) ) ;
#26737=DIRECTION ( 'NONE',  ( 0.000000000000000000, 1.000000000000000000, 0.000000000000000000 ) ) ;
#26906=CARTESIAN_POINT ( 'NONE',  ( 15.53338745080000116, -83.75000000000000000, 28.43367500519999780 ) ) ;
#26915=DIRECTION ( 'NONE',  ( 0.000000000000000000, 1.000000000000000000, 0.000000000000000000 ) ) ;
#27107=ORIENTED_EDGE ( 'NONE', *, *, #16722, .T. ) ;
#27282=ORIENTED_EDGE ( 'NONE', *, *, #14394, .F. ) ;
#27433=CARTESIAN_POINT ( 'NONE',  ( -16.73195129730000374, -83.75000000000000000, -30.62763141000000289 ) ) ;
#27568=CYLINDRICAL_SURFACE ( 'NONE', #25564, 32.39999999999999147 ) ;
#27589=CARTESIAN_POINT ( 'NONE',  ( 0.000000000000000000, 0.000000000000000000, 0.000000000000000000 ) ) ;
#27671=CARTESIAN_POINT ( 'NONE',  ( 15.53338745080000116, -84.25000000000000000, 28.43367500519999780 ) ) ;
#27810=CIRCLE ( 'NONE', #23616, 1.250000000000000000 ) ;
#27840=ORIENTED_EDGE ( 'NONE', *, *, #14394, .T. ) ;
#27884=DIRECTION ( 'NONE',  ( 0.4794255386042041156, 0.000000000000000000, 0.8775825618903722036 ) ) ;
#27932=LINE ( 'NONE', #27671, #26143 ) ;
#28128=( NAMED_UNIT ( * ) PLANE_ANGLE_UNIT ( ) SI_UNIT ( $, .RADIAN. ) );
#28166=EDGE_CURVE ( 'NONE', #8116, #5957, #27810, .T. ) ;
#28204=EDGE_LOOP ( 'NONE', ( #21819, #17195, #27840, #21044 ) ) ;
#28322=CIRCLE ( 'NONE', #19934, 34.89999999999999858 ) ;
#28551=CIRCLE ( 'NONE', #4374, 1.249999999999999112 ) ;
#28764=( NAMED_UNIT ( * ) PLANE_ANGLE_UNIT ( ) SI_UNIT ( $, .RADIAN. ) );
#28797=DIRECTION ( 'NONE',  ( 0.4794255386042040601, 0.000000000000000000, 0.8775825618903719816 ) ) ;
ENDSEC;
END-ISO-10303-21;
